ISO-10303-21;
HEADER;
/* Generated by software containing ST-Developer
 * from STEP Tools, Inc. (www.steptools.com) 
 */

FILE_DESCRIPTION(
/* description */ ('Turntable on roller ring'),
/* implementation_level */ '2;1');

FILE_NAME(
/* name */ 'Seals 2RS (1).step',
/* time_stamp */ '2026-10-28T03:23:59-07:00',
/* author */ (''),
/* organization */ (''),
/* preprocessor_version */ 'ST-DEVELOPER v20.2',
/* originating_system */ 'Autodesk Translation Framework v15.17.0.0',
/* authorisation */ '');

FILE_SCHEMA (('AUTOMOTIVE_DESIGN { 1 0 10303 214 3 1 1 }'));
ENDSEC;

DATA;
#10=MECHANICAL_DESIGN_GEOMETRIC_PRESENTATION_REPRESENTATION('',(#687,#688),#16281);
#561=SHAPE_REPRESENTATION_RELATIONSHIP('SRR','None',#16586,#616);
#616=ADVANCED_BREP_SHAPE_REPRESENTATION('',(#755,#756),#16280);
#687=STYLED_ITEM('',(#16932),#755);
#688=STYLED_ITEM('',(#16932),#756);
#755=MANIFOLD_SOLID_BREP('Body1',#8432);
#756=MANIFOLD_SOLID_BREP('Body2',#8433);
#986=FACE_BOUND('',#2482,.T.);
#987=FACE_BOUND('',#2485,.T.);
#988=FACE_BOUND('',#2488,.T.);
#989=FACE_BOUND('',#2491,.T.);
#1246=PLANE('',#10153);
#1247=PLANE('',#10158);
#1248=PLANE('',#10161);
#1249=PLANE('',#10166);
#1747=FACE_OUTER_BOUND('',#2481,.T.);
#1748=FACE_OUTER_BOUND('',#2483,.T.);
#1749=FACE_OUTER_BOUND('',#2484,.T.);
#1750=FACE_OUTER_BOUND('',#2486,.T.);
#1751=FACE_OUTER_BOUND('',#2487,.T.);
#1752=FACE_OUTER_BOUND('',#2489,.T.);
#1753=FACE_OUTER_BOUND('',#2490,.T.);
#1754=FACE_OUTER_BOUND('',#2492,.T.);
#2481=EDGE_LOOP('',(#7645));
#2482=EDGE_LOOP('',(#7646));
#2483=EDGE_LOOP('',(#7647,#7648,#7649,#7650));
#2484=EDGE_LOOP('',(#7651));
#2485=EDGE_LOOP('',(#7652));
#2486=EDGE_LOOP('',(#7653,#7654,#7655,#7656));
#2487=EDGE_LOOP('',(#7657));
#2488=EDGE_LOOP('',(#7658));
#2489=EDGE_LOOP('',(#7659,#7660,#7661,#7662));
#2490=EDGE_LOOP('',(#7663));
#2491=EDGE_LOOP('',(#7664));
#2492=EDGE_LOOP('',(#7665,#7666,#7667,#7668));
#2972=LINE('',#16093,#3455);
#2973=LINE('',#16098,#3456);
#2974=LINE('',#16107,#3457);
#2975=LINE('',#16112,#3458);
#3455=VECTOR('',#12915,1.013815);
#3456=VECTOR('',#12922,0.991185);
#3457=VECTOR('',#12933,1.013815);
#3458=VECTOR('',#12940,0.991185);
#3941=CIRCLE('',#10154,1.013815);
#3942=CIRCLE('',#10155,0.991185);
#3943=CIRCLE('',#10157,1.013815);
#3944=CIRCLE('',#10159,0.991185);
#3945=CIRCLE('',#10162,1.013815);
#3946=CIRCLE('',#10163,0.991185);
#3947=CIRCLE('',#10165,1.013815);
#3948=CIRCLE('',#10167,0.991185);
#4625=VERTEX_POINT('',#16086);
#4626=VERTEX_POINT('',#16088);
#4627=VERTEX_POINT('',#16091);
#4628=VERTEX_POINT('',#16095);
#4629=VERTEX_POINT('',#16100);
#4630=VERTEX_POINT('',#16102);
#4631=VERTEX_POINT('',#16105);
#4632=VERTEX_POINT('',#16109);
#5633=EDGE_CURVE('',#4625,#4625,#3941,.T.);
#5634=EDGE_CURVE('',#4626,#4626,#3942,.T.);
#5635=EDGE_CURVE('',#4627,#4627,#3943,.T.);
#5636=EDGE_CURVE('',#4627,#4625,#2972,.T.);
#5637=EDGE_CURVE('',#4628,#4628,#3944,.T.);
#5638=EDGE_CURVE('',#4628,#4626,#2973,.T.);
#5639=EDGE_CURVE('',#4629,#4629,#3945,.T.);
#5640=EDGE_CURVE('',#4630,#4630,#3946,.T.);
#5641=EDGE_CURVE('',#4631,#4631,#3947,.T.);
#5642=EDGE_CURVE('',#4631,#4629,#2974,.T.);
#5643=EDGE_CURVE('',#4632,#4632,#3948,.T.);
#5644=EDGE_CURVE('',#4632,#4630,#2975,.T.);
#7645=ORIENTED_EDGE('',*,*,#5633,.F.);
#7646=ORIENTED_EDGE('',*,*,#5634,.T.);
#7647=ORIENTED_EDGE('',*,*,#5635,.F.);
#7648=ORIENTED_EDGE('',*,*,#5636,.T.);
#7649=ORIENTED_EDGE('',*,*,#5633,.T.);
#7650=ORIENTED_EDGE('',*,*,#5636,.F.);
#7651=ORIENTED_EDGE('',*,*,#5635,.T.);
#7652=ORIENTED_EDGE('',*,*,#5637,.F.);
#7653=ORIENTED_EDGE('',*,*,#5637,.T.);
#7654=ORIENTED_EDGE('',*,*,#5638,.T.);
#7655=ORIENTED_EDGE('',*,*,#5634,.F.);
#7656=ORIENTED_EDGE('',*,*,#5638,.F.);
#7657=ORIENTED_EDGE('',*,*,#5639,.F.);
#7658=ORIENTED_EDGE('',*,*,#5640,.T.);
#7659=ORIENTED_EDGE('',*,*,#5641,.F.);
#7660=ORIENTED_EDGE('',*,*,#5642,.T.);
#7661=ORIENTED_EDGE('',*,*,#5639,.T.);
#7662=ORIENTED_EDGE('',*,*,#5642,.F.);
#7663=ORIENTED_EDGE('',*,*,#5641,.T.);
#7664=ORIENTED_EDGE('',*,*,#5643,.F.);
#7665=ORIENTED_EDGE('',*,*,#5643,.T.);
#7666=ORIENTED_EDGE('',*,*,#5644,.T.);
#7667=ORIENTED_EDGE('',*,*,#5640,.F.);
#7668=ORIENTED_EDGE('',*,*,#5644,.F.);
#7849=CYLINDRICAL_SURFACE('',#10156,1.013815);
#7850=CYLINDRICAL_SURFACE('',#10160,0.991185);
#7851=CYLINDRICAL_SURFACE('',#10164,1.013815);
#7852=CYLINDRICAL_SURFACE('',#10168,0.991185);
#8350=ADVANCED_FACE('',(#1747,#986),#1246,.T.);
#8351=ADVANCED_FACE('',(#1748),#7849,.T.);
#8352=ADVANCED_FACE('',(#1749,#987),#1247,.T.);
#8353=ADVANCED_FACE('',(#1750),#7850,.F.);
#8354=ADVANCED_FACE('',(#1751,#988),#1248,.T.);
#8355=ADVANCED_FACE('',(#1752),#7851,.T.);
#8356=ADVANCED_FACE('',(#1753,#989),#1249,.T.);
#8357=ADVANCED_FACE('',(#1754),#7852,.F.);
#8432=CLOSED_SHELL('',(#8350,#8351,#8352,#8353));
#8433=CLOSED_SHELL('',(#8354,#8355,#8356,#8357));
#10152=AXIS2_PLACEMENT_3D('',#16084,#12903,#12904);
#10153=AXIS2_PLACEMENT_3D('',#16085,#12905,#12906);
#10154=AXIS2_PLACEMENT_3D('',#16087,#12907,#12908);
#10155=AXIS2_PLACEMENT_3D('',#16089,#12909,#12910);
#10156=AXIS2_PLACEMENT_3D('',#16090,#12911,#12912);
#10157=AXIS2_PLACEMENT_3D('',#16092,#12913,#12914);
#10158=AXIS2_PLACEMENT_3D('',#16094,#12916,#12917);
#10159=AXIS2_PLACEMENT_3D('',#16096,#12918,#12919);
#10160=AXIS2_PLACEMENT_3D('',#16097,#12920,#12921);
#10161=AXIS2_PLACEMENT_3D('',#16099,#12923,#12924);
#10162=AXIS2_PLACEMENT_3D('',#16101,#12925,#12926);
#10163=AXIS2_PLACEMENT_3D('',#16103,#12927,#12928);
#10164=AXIS2_PLACEMENT_3D('',#16104,#12929,#12930);
#10165=AXIS2_PLACEMENT_3D('',#16106,#12931,#12932);
#10166=AXIS2_PLACEMENT_3D('',#16108,#12934,#12935);
#10167=AXIS2_PLACEMENT_3D('',#16110,#12936,#12937);
#10168=AXIS2_PLACEMENT_3D('',#16111,#12938,#12939);
#12903=DIRECTION('axis',(0.,0.,1.));
#12904=DIRECTION('refdir',(1.,0.,0.));
#12905=DIRECTION('center_axis',(0.,1.,0.));
#12906=DIRECTION('ref_axis',(0.,0.,1.));
#12907=DIRECTION('center_axis',(0.,-1.,0.));
#12908=DIRECTION('ref_axis',(1.,0.,0.));
#12909=DIRECTION('center_axis',(0.,-1.,0.));
#12910=DIRECTION('ref_axis',(1.,0.,0.));
#12911=DIRECTION('center_axis',(0.,-1.,0.));
#12912=DIRECTION('ref_axis',(1.,0.,0.));
#12913=DIRECTION('center_axis',(0.,-1.,0.));
#12914=DIRECTION('ref_axis',(1.,0.,0.));
#12915=DIRECTION('',(0.,1.,0.));
#12916=DIRECTION('center_axis',(0.,-1.,0.));
#12917=DIRECTION('ref_axis',(0.,0.,-1.));
#12918=DIRECTION('center_axis',(0.,-1.,0.));
#12919=DIRECTION('ref_axis',(1.,0.,0.));
#12920=DIRECTION('center_axis',(0.,-1.,0.));
#12921=DIRECTION('ref_axis',(1.,0.,0.));
#12922=DIRECTION('',(0.,1.,0.));
#12923=DIRECTION('center_axis',(0.,1.,0.));
#12924=DIRECTION('ref_axis',(0.,0.,1.));
#12925=DIRECTION('center_axis',(0.,-1.,0.));
#12926=DIRECTION('ref_axis',(1.,0.,0.));
#12927=DIRECTION('center_axis',(0.,-1.,0.));
#12928=DIRECTION('ref_axis',(1.,0.,0.));
#12929=DIRECTION('center_axis',(0.,-1.,0.));
#12930=DIRECTION('ref_axis',(1.,0.,0.));
#12931=DIRECTION('center_axis',(0.,-1.,0.));
#12932=DIRECTION('ref_axis',(1.,0.,0.));
#12933=DIRECTION('',(0.,1.,0.));
#12934=DIRECTION('center_axis',(0.,-1.,0.));
#12935=DIRECTION('ref_axis',(0.,0.,-1.));
#12936=DIRECTION('center_axis',(0.,-1.,0.));
#12937=DIRECTION('ref_axis',(1.,0.,0.));
#12938=DIRECTION('center_axis',(0.,-1.,0.));
#12939=DIRECTION('ref_axis',(1.,0.,0.));
#12940=DIRECTION('',(0.,1.,0.));
#16084=CARTESIAN_POINT('',(0.,0.,0.));
#16085=CARTESIAN_POINT('Origin',(1.013815,0.445,0.));
#16086=CARTESIAN_POINT('',(-1.013815,0.445,-1.24156529467757E-16));
#16087=CARTESIAN_POINT('Origin',(0.,0.445,0.));
#16088=CARTESIAN_POINT('',(-0.991185,0.445,-1.21385153761287E-16));
#16089=CARTESIAN_POINT('Origin',(0.,0.445,0.));
#16090=CARTESIAN_POINT('Origin',(0.,0.4075,0.));
#16091=CARTESIAN_POINT('',(-1.013815,0.37,-1.24156529467757E-16));
#16092=CARTESIAN_POINT('Origin',(0.,0.37,0.));
#16093=CARTESIAN_POINT('',(-1.013815,0.4075,-1.24156529467757E-16));
#16094=CARTESIAN_POINT('Origin',(0.991185,0.37,0.));
#16095=CARTESIAN_POINT('',(-0.991185,0.37,-1.21385153761287E-16));
#16096=CARTESIAN_POINT('Origin',(0.,0.37,0.));
#16097=CARTESIAN_POINT('Origin',(0.,0.4075,0.));
#16098=CARTESIAN_POINT('',(-0.991185,0.4075,-1.21385153761287E-16));
#16099=CARTESIAN_POINT('Origin',(1.013815,-0.37,0.));
#16100=CARTESIAN_POINT('',(-1.013815,-0.37,-1.24156529467757E-16));
#16101=CARTESIAN_POINT('Origin',(0.,-0.37,0.));
#16102=CARTESIAN_POINT('',(-0.991185,-0.37,-1.21385153761287E-16));
#16103=CARTESIAN_POINT('Origin',(0.,-0.37,0.));
#16104=CARTESIAN_POINT('Origin',(0.,-0.4075,0.));
#16105=CARTESIAN_POINT('',(-1.013815,-0.445,-1.24156529467757E-16));
#16106=CARTESIAN_POINT('Origin',(0.,-0.445,0.));
#16107=CARTESIAN_POINT('',(-1.013815,-0.4075,-1.24156529467757E-16));
#16108=CARTESIAN_POINT('Origin',(0.991185,-0.445,0.));
#16109=CARTESIAN_POINT('',(-0.991185,-0.445,-1.21385153761287E-16));
#16110=CARTESIAN_POINT('Origin',(0.,-0.445,0.));
#16111=CARTESIAN_POINT('Origin',(0.,-0.4075,0.));
#16112=CARTESIAN_POINT('',(-0.991185,-0.4075,-1.21385153761287E-16));
#16211=UNCERTAINTY_MEASURE_WITH_UNIT(LENGTH_MEASURE(0.001),#16282,
'DISTANCE_ACCURACY_VALUE',
'Maximum model space distance between geometric entities at asserted c
onnectivities');
#16212=UNCERTAINTY_MEASURE_WITH_UNIT(LENGTH_MEASURE(0.001),#16282,
'DISTANCE_ACCURACY_VALUE',
'Maximum model space distance between geometric entities at asserted c
onnectivities');
#16280=(
GEOMETRIC_REPRESENTATION_CONTEXT(3)
GLOBAL_UNCERTAINTY_ASSIGNED_CONTEXT((#16211))
GLOBAL_UNIT_ASSIGNED_CONTEXT((#16282,#16284,#16285))
REPRESENTATION_CONTEXT('','3D')
);
#16281=(
GEOMETRIC_REPRESENTATION_CONTEXT(3)
GLOBAL_UNCERTAINTY_ASSIGNED_CONTEXT((#16212))
GLOBAL_UNIT_ASSIGNED_CONTEXT((#16282,#16284,#16285))
REPRESENTATION_CONTEXT('','3D')
);
#16282=(
LENGTH_UNIT()
NAMED_UNIT(*)
SI_UNIT(.CENTI.,.METRE.)
);
#16284=(
NAMED_UNIT(*)
PLANE_ANGLE_UNIT()
SI_UNIT($,.RADIAN.)
);
#16285=(
NAMED_UNIT(*)
SI_UNIT($,.STERADIAN.)
SOLID_ANGLE_UNIT()
);
#16353=SHAPE_DEFINITION_REPRESENTATION(#16487,#16586);
#16487=PRODUCT_DEFINITION_SHAPE('',$,#16655);
#16586=SHAPE_REPRESENTATION('',(#10152),#16280);
#16587=PRODUCT_DEFINITION_CONTEXT('part definition',#16793,'design');
#16655=PRODUCT_DEFINITION('Seals 2RS (1)','Seals 2RS (1)',#16723,#16587);
#16723=PRODUCT_DEFINITION_FORMATION('',$,#16862);
#16793=APPLICATION_CONTEXT(
'Core Data for Automotive Mechanical Design Process');
#16794=PRODUCT_CONTEXT('part definition',#16793,'mechanical');
#16862=PRODUCT('Seals 2RS (1)','Seals 2RS (1)','Seals 2RS (1)',(#16794));
#16926=COLOUR_RGB('Grey',0.48,0.52,0.57);
#16927=FILL_AREA_STYLE_COLOUR('',#16926);
#16928=FILL_AREA_STYLE('',(#16927));
#16929=SURFACE_STYLE_FILL_AREA(#16928);
#16930=SURFACE_SIDE_STYLE('',(#16929));
#16931=SURFACE_STYLE_USAGE(.BOTH.,#16930);
#16932=PRESENTATION_STYLE_ASSIGNMENT((#16931));
ENDSEC;
END-ISO-10303-21;
